ISO-10303-21;
HEADER;
/* Generated by software containing ST-Developer
 * from STEP Tools, Inc. (www.steptools.com) 
 */

FILE_DESCRIPTION(
/* description */ ('STEP AP214'),
/* implementation_level */ '2;1');

FILE_NAME(
/* name */ 'PRT-TQ1012-10.step',
/* time_stamp */ '2026-10-07T12:49:37-07:00',
/* author */ (''),
/* organization */ (''),
/* preprocessor_version */ 'ST-DEVELOPER v20.2',
/* originating_system */ 'Autodesk Translation Framework v15.15.0.0',
/* authorisation */ '');

FILE_SCHEMA (('AUTOMOTIVE_DESIGN { 1 0 10303 214 3 1 1 }'));
ENDSEC;

DATA;
#10=MECHANICAL_DESIGN_GEOMETRIC_PRESENTATION_REPRESENTATION('',(#298),#33016);
#178=SPHERICAL_SURFACE('',#10791,1.75);
#244=SHAPE_REPRESENTATION_RELATIONSHIP('SRR','None',#33138,#271);
#271=ADVANCED_BREP_SHAPE_REPRESENTATION('',(#329),#32999);
#298=STYLED_ITEM('',(#33289),#329);
#329=MANIFOLD_SOLID_BREP('Body1',#9953);
#359=CONICAL_SURFACE('',#10797,2.4455,0.785398163397455);
#390=TOROIDAL_SURFACE('',#10793,4.5,0.5);
#514=FACE_BOUND('',#1923,.T.);
#515=FACE_BOUND('',#1926,.T.);
#516=FACE_BOUND('',#1939,.T.);
#904=PLANE('',#10783);
#905=PLANE('',#10788);
#906=PLANE('',#10799);
#907=PLANE('',#10800);
#908=PLANE('',#10801);
#909=PLANE('',#10802);
#910=PLANE('',#10803);
#911=PLANE('',#10804);
#912=PLANE('',#10805);
#913=PLANE('',#10806);
#1326=FACE_OUTER_BOUND('',#1922,.T.);
#1327=FACE_OUTER_BOUND('',#1924,.T.);
#1328=FACE_OUTER_BOUND('',#1925,.T.);
#1329=FACE_OUTER_BOUND('',#1927,.T.);
#1330=FACE_OUTER_BOUND('',#1928,.T.);
#1331=FACE_OUTER_BOUND('',#1929,.T.);
#1332=FACE_OUTER_BOUND('',#1930,.T.);
#1333=FACE_OUTER_BOUND('',#1931,.T.);
#1334=FACE_OUTER_BOUND('',#1932,.T.);
#1335=FACE_OUTER_BOUND('',#1933,.T.);
#1336=FACE_OUTER_BOUND('',#1934,.T.);
#1337=FACE_OUTER_BOUND('',#1935,.T.);
#1338=FACE_OUTER_BOUND('',#1936,.T.);
#1339=FACE_OUTER_BOUND('',#1937,.T.);
#1340=FACE_OUTER_BOUND('',#1938,.T.);
#1922=EDGE_LOOP('',(#8008));
#1923=EDGE_LOOP('',(#8009));
#1924=EDGE_LOOP('',(#8010,#8011,#8012,#8013));
#1925=EDGE_LOOP('',(#8014));
#1926=EDGE_LOOP('',(#8015));
#1927=EDGE_LOOP('',(#8016,#8017,#8018));
#1928=EDGE_LOOP('',(#8019,#8020,#8021,#8022));
#1929=EDGE_LOOP('',(#8023,#8024,#8025,#8026));
#1930=EDGE_LOOP('',(#8027,#8028,#8029,#8030));
#1931=EDGE_LOOP('',(#8031,#8032,#8033,#8034,#8035,#8036));
#1932=EDGE_LOOP('',(#8037,#8038,#8039,#8040));
#1933=EDGE_LOOP('',(#8041,#8042,#8043,#8044));
#1934=EDGE_LOOP('',(#8045,#8046,#8047,#8048));
#1935=EDGE_LOOP('',(#8049,#8050,#8051,#8052));
#1936=EDGE_LOOP('',(#8053,#8054,#8055,#8056));
#1937=EDGE_LOOP('',(#8057,#8058,#8059,#8060));
#1938=EDGE_LOOP('',(#8061));
#1939=EDGE_LOOP('',(#8062,#8063,#8064,#8065,#8066,#8067));
#2440=CIRCLE('',#10784,5.);
#2441=CIRCLE('',#10785,3.);
#2442=CIRCLE('',#10787,5.);
#2443=CIRCLE('',#10789,4.5);
#2444=CIRCLE('',#10790,1.75);
#2445=CIRCLE('',#10792,1.75);
#2446=CIRCLE('',#10794,0.5);
#2447=CIRCLE('',#10796,3.);
#2448=CIRCLE('',#10798,2.4455);
#3056=LINE('',#23891,#3806);
#3057=LINE('',#23905,#3807);
#3058=LINE('',#23909,#3808);
#3059=LINE('',#23914,#3809);
#3060=LINE('',#23916,#3810);
#3061=LINE('',#23918,#3811);
#3062=LINE('',#23920,#3812);
#3063=LINE('',#23922,#3813);
#3064=LINE('',#23923,#3814);
#3065=LINE('',#23927,#3815);
#3066=LINE('',#23928,#3816);
#3067=LINE('',#23929,#3817);
#3068=LINE('',#23932,#3818);
#3069=LINE('',#23933,#3819);
#3070=LINE('',#23936,#3820);
#3071=LINE('',#23937,#3821);
#3072=LINE('',#23940,#3822);
#3073=LINE('',#23941,#3823);
#3074=LINE('',#23944,#3824);
#3075=LINE('',#23945,#3825);
#3076=LINE('',#23947,#3826);
#3806=VECTOR('',#12729,5.);
#3807=VECTOR('',#12748,3.);
#3808=VECTOR('',#12753,2.4455);
#3809=VECTOR('',#12758,1000.);
#3810=VECTOR('',#12759,1000.);
#3811=VECTOR('',#12760,1000.);
#3812=VECTOR('',#12761,1000.);
#3813=VECTOR('',#12762,1000.);
#3814=VECTOR('',#12763,1000.);
#3815=VECTOR('',#12766,1000.);
#3816=VECTOR('',#12767,1000.);
#3817=VECTOR('',#12768,1000.);
#3818=VECTOR('',#12771,1000.);
#3819=VECTOR('',#12772,1000.);
#3820=VECTOR('',#12775,1000.);
#3821=VECTOR('',#12776,1000.);
#3822=VECTOR('',#12779,1000.);
#3823=VECTOR('',#12780,1000.);
#3824=VECTOR('',#12783,1000.);
#3825=VECTOR('',#12784,1000.);
#3826=VECTOR('',#12787,1000.);
#4620=VERTEX_POINT('',#23885);
#4621=VERTEX_POINT('',#23887);
#4622=VERTEX_POINT('',#23890);
#4623=VERTEX_POINT('',#23894);
#4624=VERTEX_POINT('',#23896);
#4625=VERTEX_POINT('',#23899);
#4626=VERTEX_POINT('',#23904);
#4627=VERTEX_POINT('',#23908);
#4628=VERTEX_POINT('',#23912);
#4629=VERTEX_POINT('',#23913);
#4630=VERTEX_POINT('',#23915);
#4631=VERTEX_POINT('',#23917);
#4632=VERTEX_POINT('',#23919);
#4633=VERTEX_POINT('',#23921);
#4634=VERTEX_POINT('',#23925);
#4635=VERTEX_POINT('',#23926);
#4636=VERTEX_POINT('',#23931);
#4637=VERTEX_POINT('',#23935);
#4638=VERTEX_POINT('',#23939);
#4639=VERTEX_POINT('',#23943);
#5817=EDGE_CURVE('',#4620,#4620,#2440,.T.);
#5818=EDGE_CURVE('',#4621,#4621,#2441,.T.);
#5819=EDGE_CURVE('',#4620,#4622,#3056,.T.);
#5820=EDGE_CURVE('',#4622,#4622,#2442,.T.);
#5821=EDGE_CURVE('',#4623,#4623,#2443,.T.);
#5822=EDGE_CURVE('',#4624,#4624,#2444,.T.);
#5823=EDGE_CURVE('',#4625,#4624,#2445,.T.);
#5824=EDGE_CURVE('',#4622,#4623,#2446,.T.);
#5825=EDGE_CURVE('',#4621,#4626,#3057,.T.);
#5826=EDGE_CURVE('',#4626,#4626,#2447,.T.);
#5827=EDGE_CURVE('',#4626,#4627,#3058,.T.);
#5828=EDGE_CURVE('',#4627,#4627,#2448,.T.);
#5829=EDGE_CURVE('',#4628,#4629,#3059,.T.);
#5830=EDGE_CURVE('',#4629,#4630,#3060,.T.);
#5831=EDGE_CURVE('',#4630,#4631,#3061,.T.);
#5832=EDGE_CURVE('',#4631,#4632,#3062,.T.);
#5833=EDGE_CURVE('',#4632,#4633,#3063,.T.);
#5834=EDGE_CURVE('',#4633,#4628,#3064,.T.);
#5835=EDGE_CURVE('',#4634,#4635,#3065,.T.);
#5836=EDGE_CURVE('',#4631,#4635,#3066,.T.);
#5837=EDGE_CURVE('',#4630,#4634,#3067,.T.);
#5838=EDGE_CURVE('',#4635,#4636,#3068,.T.);
#5839=EDGE_CURVE('',#4632,#4636,#3069,.T.);
#5840=EDGE_CURVE('',#4636,#4637,#3070,.T.);
#5841=EDGE_CURVE('',#4633,#4637,#3071,.T.);
#5842=EDGE_CURVE('',#4637,#4638,#3072,.T.);
#5843=EDGE_CURVE('',#4628,#4638,#3073,.T.);
#5844=EDGE_CURVE('',#4638,#4639,#3074,.T.);
#5845=EDGE_CURVE('',#4629,#4639,#3075,.T.);
#5846=EDGE_CURVE('',#4639,#4634,#3076,.T.);
#8008=ORIENTED_EDGE('',*,*,#5817,.T.);
#8009=ORIENTED_EDGE('',*,*,#5818,.T.);
#8010=ORIENTED_EDGE('',*,*,#5817,.F.);
#8011=ORIENTED_EDGE('',*,*,#5819,.T.);
#8012=ORIENTED_EDGE('',*,*,#5820,.T.);
#8013=ORIENTED_EDGE('',*,*,#5819,.F.);
#8014=ORIENTED_EDGE('',*,*,#5821,.T.);
#8015=ORIENTED_EDGE('',*,*,#5822,.T.);
#8016=ORIENTED_EDGE('',*,*,#5822,.F.);
#8017=ORIENTED_EDGE('',*,*,#5823,.F.);
#8018=ORIENTED_EDGE('',*,*,#5823,.T.);
#8019=ORIENTED_EDGE('',*,*,#5820,.F.);
#8020=ORIENTED_EDGE('',*,*,#5824,.T.);
#8021=ORIENTED_EDGE('',*,*,#5821,.F.);
#8022=ORIENTED_EDGE('',*,*,#5824,.F.);
#8023=ORIENTED_EDGE('',*,*,#5818,.F.);
#8024=ORIENTED_EDGE('',*,*,#5825,.T.);
#8025=ORIENTED_EDGE('',*,*,#5826,.T.);
#8026=ORIENTED_EDGE('',*,*,#5825,.F.);
#8027=ORIENTED_EDGE('',*,*,#5826,.F.);
#8028=ORIENTED_EDGE('',*,*,#5827,.T.);
#8029=ORIENTED_EDGE('',*,*,#5828,.T.);
#8030=ORIENTED_EDGE('',*,*,#5827,.F.);
#8031=ORIENTED_EDGE('',*,*,#5829,.T.);
#8032=ORIENTED_EDGE('',*,*,#5830,.T.);
#8033=ORIENTED_EDGE('',*,*,#5831,.T.);
#8034=ORIENTED_EDGE('',*,*,#5832,.T.);
#8035=ORIENTED_EDGE('',*,*,#5833,.T.);
#8036=ORIENTED_EDGE('',*,*,#5834,.T.);
#8037=ORIENTED_EDGE('',*,*,#5835,.T.);
#8038=ORIENTED_EDGE('',*,*,#5836,.F.);
#8039=ORIENTED_EDGE('',*,*,#5831,.F.);
#8040=ORIENTED_EDGE('',*,*,#5837,.T.);
#8041=ORIENTED_EDGE('',*,*,#5838,.T.);
#8042=ORIENTED_EDGE('',*,*,#5839,.F.);
#8043=ORIENTED_EDGE('',*,*,#5832,.F.);
#8044=ORIENTED_EDGE('',*,*,#5836,.T.);
#8045=ORIENTED_EDGE('',*,*,#5840,.T.);
#8046=ORIENTED_EDGE('',*,*,#5841,.F.);
#8047=ORIENTED_EDGE('',*,*,#5833,.F.);
#8048=ORIENTED_EDGE('',*,*,#5839,.T.);
#8049=ORIENTED_EDGE('',*,*,#5842,.T.);
#8050=ORIENTED_EDGE('',*,*,#5843,.F.);
#8051=ORIENTED_EDGE('',*,*,#5834,.F.);
#8052=ORIENTED_EDGE('',*,*,#5841,.T.);
#8053=ORIENTED_EDGE('',*,*,#5844,.T.);
#8054=ORIENTED_EDGE('',*,*,#5845,.F.);
#8055=ORIENTED_EDGE('',*,*,#5829,.F.);
#8056=ORIENTED_EDGE('',*,*,#5843,.T.);
#8057=ORIENTED_EDGE('',*,*,#5846,.T.);
#8058=ORIENTED_EDGE('',*,*,#5837,.F.);
#8059=ORIENTED_EDGE('',*,*,#5830,.F.);
#8060=ORIENTED_EDGE('',*,*,#5845,.T.);
#8061=ORIENTED_EDGE('',*,*,#5828,.F.);
#8062=ORIENTED_EDGE('',*,*,#5846,.F.);
#8063=ORIENTED_EDGE('',*,*,#5844,.F.);
#8064=ORIENTED_EDGE('',*,*,#5842,.F.);
#8065=ORIENTED_EDGE('',*,*,#5840,.F.);
#8066=ORIENTED_EDGE('',*,*,#5838,.F.);
#8067=ORIENTED_EDGE('',*,*,#5835,.F.);
#9311=CYLINDRICAL_SURFACE('',#10786,5.);
#9312=CYLINDRICAL_SURFACE('',#10795,3.);
#9692=ADVANCED_FACE('',(#1326,#514),#904,.F.);
#9693=ADVANCED_FACE('',(#1327),#9311,.T.);
#9694=ADVANCED_FACE('',(#1328,#515),#905,.F.);
#9695=ADVANCED_FACE('',(#1329),#178,.T.);
#9696=ADVANCED_FACE('',(#1330),#390,.T.);
#9697=ADVANCED_FACE('',(#1331),#9312,.T.);
#9698=ADVANCED_FACE('',(#1332),#359,.T.);
#9699=ADVANCED_FACE('',(#1333),#906,.T.);
#9700=ADVANCED_FACE('',(#1334),#907,.F.);
#9701=ADVANCED_FACE('',(#1335),#908,.F.);
#9702=ADVANCED_FACE('',(#1336),#909,.F.);
#9703=ADVANCED_FACE('',(#1337),#910,.F.);
#9704=ADVANCED_FACE('',(#1338),#911,.F.);
#9705=ADVANCED_FACE('',(#1339),#912,.F.);
#9706=ADVANCED_FACE('',(#1340,#516),#913,.F.);
#9953=CLOSED_SHELL('',(#9692,#9693,#9694,#9695,#9696,#9697,#9698,#9699,
#9700,#9701,#9702,#9703,#9704,#9705,#9706));
#10782=AXIS2_PLACEMENT_3D('',#23883,#12719,#12720);
#10783=AXIS2_PLACEMENT_3D('',#23884,#12721,#12722);
#10784=AXIS2_PLACEMENT_3D('',#23886,#12723,#12724);
#10785=AXIS2_PLACEMENT_3D('',#23888,#12725,#12726);
#10786=AXIS2_PLACEMENT_3D('',#23889,#12727,#12728);
#10787=AXIS2_PLACEMENT_3D('',#23892,#12730,#12731);
#10788=AXIS2_PLACEMENT_3D('',#23893,#12732,#12733);
#10789=AXIS2_PLACEMENT_3D('',#23895,#12734,#12735);
#10790=AXIS2_PLACEMENT_3D('',#23897,#12736,#12737);
#10791=AXIS2_PLACEMENT_3D('',#23898,#12738,#12739);
#10792=AXIS2_PLACEMENT_3D('',#23900,#12740,#12741);
#10793=AXIS2_PLACEMENT_3D('',#23901,#12742,#12743);
#10794=AXIS2_PLACEMENT_3D('',#23902,#12744,#12745);
#10795=AXIS2_PLACEMENT_3D('',#23903,#12746,#12747);
#10796=AXIS2_PLACEMENT_3D('',#23906,#12749,#12750);
#10797=AXIS2_PLACEMENT_3D('',#23907,#12751,#12752);
#10798=AXIS2_PLACEMENT_3D('',#23910,#12754,#12755);
#10799=AXIS2_PLACEMENT_3D('',#23911,#12756,#12757);
#10800=AXIS2_PLACEMENT_3D('',#23924,#12764,#12765);
#10801=AXIS2_PLACEMENT_3D('',#23930,#12769,#12770);
#10802=AXIS2_PLACEMENT_3D('',#23934,#12773,#12774);
#10803=AXIS2_PLACEMENT_3D('',#23938,#12777,#12778);
#10804=AXIS2_PLACEMENT_3D('',#23942,#12781,#12782);
#10805=AXIS2_PLACEMENT_3D('',#23946,#12785,#12786);
#10806=AXIS2_PLACEMENT_3D('',#23948,#12788,#12789);
#12719=DIRECTION('axis',(0.,0.,1.));
#12720=DIRECTION('refdir',(1.,0.,0.));
#12721=DIRECTION('center_axis',(0.,1.,0.));
#12722=DIRECTION('ref_axis',(0.,0.,1.));
#12723=DIRECTION('center_axis',(0.,-1.,0.));
#12724=DIRECTION('ref_axis',(0.,0.,-1.));
#12725=DIRECTION('center_axis',(0.,1.,0.));
#12726=DIRECTION('ref_axis',(0.,0.,1.));
#12727=DIRECTION('center_axis',(0.,-1.,0.));
#12728=DIRECTION('ref_axis',(0.,0.,-1.));
#12729=DIRECTION('',(0.,1.,0.));
#12730=DIRECTION('center_axis',(0.,-1.,0.));
#12731=DIRECTION('ref_axis',(0.,0.,-1.));
#12732=DIRECTION('center_axis',(0.,-1.,0.));
#12733=DIRECTION('ref_axis',(0.,0.,-1.));
#12734=DIRECTION('center_axis',(0.,1.,0.));
#12735=DIRECTION('ref_axis',(0.,0.,-1.));
#12736=DIRECTION('center_axis',(0.,-1.,0.));
#12737=DIRECTION('ref_axis',(0.,0.,-1.));
#12738=DIRECTION('center_axis',(0.,1.,-6.12323399573677E-17));
#12739=DIRECTION('ref_axis',(0.,0.,-1.));
#12740=DIRECTION('center_axis',(1.,0.,-1.22464679914735E-16));
#12741=DIRECTION('ref_axis',(1.22464679914735E-16,0.,1.));
#12742=DIRECTION('center_axis',(0.,-1.,0.));
#12743=DIRECTION('ref_axis',(0.,0.,-1.));
#12744=DIRECTION('center_axis',(-1.,0.,-1.22464679914735E-16));
#12745=DIRECTION('ref_axis',(-1.22464679914735E-16,0.,1.));
#12746=DIRECTION('center_axis',(0.,1.,0.));
#12747=DIRECTION('ref_axis',(0.,0.,1.));
#12748=DIRECTION('',(0.,-1.,0.));
#12749=DIRECTION('center_axis',(0.,1.,0.));
#12750=DIRECTION('ref_axis',(0.,0.,1.));
#12751=DIRECTION('center_axis',(0.,1.,0.));
#12752=DIRECTION('ref_axis',(0.,0.,1.));
#12753=DIRECTION('',(8.65956056235499E-17,-0.707106781186542,0.707106781186553));
#12754=DIRECTION('center_axis',(0.,1.,0.));
#12755=DIRECTION('ref_axis',(0.,0.,1.));
#12756=DIRECTION('center_axis',(0.,-1.,0.));
#12757=DIRECTION('ref_axis',(0.,0.,-1.));
#12758=DIRECTION('',(-0.866025403784438,0.,0.5));
#12759=DIRECTION('',(-0.866025403784439,0.,-0.5));
#12760=DIRECTION('',(0.,0.,-1.));
#12761=DIRECTION('',(0.866025403784438,0.,-0.5));
#12762=DIRECTION('',(0.866025403784439,0.,0.5));
#12763=DIRECTION('',(0.,0.,1.));
#12764=DIRECTION('center_axis',(-1.,0.,0.));
#12765=DIRECTION('ref_axis',(0.,0.,1.));
#12766=DIRECTION('',(0.,0.,-1.));
#12767=DIRECTION('',(0.,-1.,0.));
#12768=DIRECTION('',(0.,-1.,0.));
#12769=DIRECTION('center_axis',(-0.5,0.,-0.866025403784439));
#12770=DIRECTION('ref_axis',(-0.866025403784439,0.,0.5));
#12771=DIRECTION('',(0.866025403784438,0.,-0.5));
#12772=DIRECTION('',(0.,-1.,0.));
#12773=DIRECTION('center_axis',(0.5,0.,-0.866025403784439));
#12774=DIRECTION('ref_axis',(-0.866025403784439,0.,-0.5));
#12775=DIRECTION('',(0.866025403784439,0.,0.5));
#12776=DIRECTION('',(0.,-1.,0.));
#12777=DIRECTION('center_axis',(1.,0.,0.));
#12778=DIRECTION('ref_axis',(0.,0.,-1.));
#12779=DIRECTION('',(0.,0.,1.));
#12780=DIRECTION('',(0.,-1.,0.));
#12781=DIRECTION('center_axis',(0.5,0.,0.866025403784439));
#12782=DIRECTION('ref_axis',(0.866025403784439,0.,-0.5));
#12783=DIRECTION('',(-0.866025403784438,0.,0.5));
#12784=DIRECTION('',(0.,-1.,0.));
#12785=DIRECTION('center_axis',(-0.5,0.,0.866025403784439));
#12786=DIRECTION('ref_axis',(0.866025403784439,0.,0.5));
#12787=DIRECTION('',(-0.866025403784439,0.,-0.5));
#12788=DIRECTION('center_axis',(0.,1.,0.));
#12789=DIRECTION('ref_axis',(0.,0.,1.));
#23883=CARTESIAN_POINT('',(0.,0.,0.));
#23884=CARTESIAN_POINT('Origin',(-5.,74.6,0.));
#23885=CARTESIAN_POINT('',(-6.12323399573677E-16,74.6,5.));
#23886=CARTESIAN_POINT('Origin',(0.,74.6,0.));
#23887=CARTESIAN_POINT('',(-3.67394039744206E-16,74.6,-3.));
#23888=CARTESIAN_POINT('Origin',(0.,74.6,0.));
#23889=CARTESIAN_POINT('Origin',(0.,0.,0.));
#23890=CARTESIAN_POINT('',(-6.12323399573677E-16,76.5,5.));
#23891=CARTESIAN_POINT('',(-6.12323399573677E-16,0.,5.));
#23892=CARTESIAN_POINT('Origin',(0.,76.5,0.));
#23893=CARTESIAN_POINT('Origin',(-1.75,77.,0.));
#23894=CARTESIAN_POINT('',(-5.51091059616309E-16,77.,4.5));
#23895=CARTESIAN_POINT('Origin',(0.,77.,0.));
#23896=CARTESIAN_POINT('',(2.14313189850787E-16,77.,1.75));
#23897=CARTESIAN_POINT('Origin',(0.,77.,0.));
#23898=CARTESIAN_POINT('Origin',(0.,77.,0.));
#23899=CARTESIAN_POINT('',(1.31228980982913E-32,78.75,1.07156594925393E-16));
#23900=CARTESIAN_POINT('Origin',(0.,77.,0.));
#23901=CARTESIAN_POINT('Origin',(0.,76.5,0.));
#23902=CARTESIAN_POINT('Origin',(-5.51091059616309E-16,76.5,4.5));
#23903=CARTESIAN_POINT('Origin',(0.,0.,0.));
#23904=CARTESIAN_POINT('',(-3.67394039744206E-16,0.554499999999991,-3.));
#23905=CARTESIAN_POINT('',(-3.67394039744206E-16,0.,-3.));
#23906=CARTESIAN_POINT('Origin',(0.,0.554499999999991,0.));
#23907=CARTESIAN_POINT('Origin',(0.,0.,0.));
#23908=CARTESIAN_POINT('',(-2.99487374731485E-16,-3.66766254849957E-32,
-2.4455));
#23909=CARTESIAN_POINT('',(-2.99487374731485E-16,0.,-2.4455));
#23910=CARTESIAN_POINT('Origin',(0.,0.,0.));
#23911=CARTESIAN_POINT('Origin',(0.,4.5,0.));
#23912=CARTESIAN_POINT('',(2.,4.5,1.15470053837925));
#23913=CARTESIAN_POINT('',(4.86323526963846E-16,4.5,2.3094010767585));
#23914=CARTESIAN_POINT('',(2.,4.5,1.15470053837925));
#23915=CARTESIAN_POINT('',(-2.,4.5,1.15470053837925));
#23916=CARTESIAN_POINT('',(4.86323526963846E-16,4.5,2.3094010767585));
#23917=CARTESIAN_POINT('',(-2.,4.5,-1.15470053837925));
#23918=CARTESIAN_POINT('',(-2.,4.5,1.15470053837925));
#23919=CARTESIAN_POINT('',(2.07283766416844E-16,4.5,-2.3094010767585));
#23920=CARTESIAN_POINT('',(-2.,4.5,-1.15470053837925));
#23921=CARTESIAN_POINT('',(2.,4.5,-1.15470053837925));
#23922=CARTESIAN_POINT('',(2.07283766416844E-16,4.5,-2.3094010767585));
#23923=CARTESIAN_POINT('',(2.,4.5,-1.15470053837925));
#23924=CARTESIAN_POINT('Origin',(-2.,4.5,1.15470053837925));
#23925=CARTESIAN_POINT('',(-2.,0.,1.15470053837925));
#23926=CARTESIAN_POINT('',(-2.,0.,-1.15470053837925));
#23927=CARTESIAN_POINT('',(-2.,0.,1.15470053837925));
#23928=CARTESIAN_POINT('',(-2.,4.5,-1.15470053837925));
#23929=CARTESIAN_POINT('',(-2.,4.5,1.15470053837925));
#23930=CARTESIAN_POINT('Origin',(-2.,4.5,-1.15470053837925));
#23931=CARTESIAN_POINT('',(2.07283766416844E-16,0.,-2.3094010767585));
#23932=CARTESIAN_POINT('',(-2.,0.,-1.15470053837925));
#23933=CARTESIAN_POINT('',(2.07283766416844E-16,4.5,-2.3094010767585));
#23934=CARTESIAN_POINT('Origin',(2.07283766416844E-16,4.5,-2.3094010767585));
#23935=CARTESIAN_POINT('',(2.,0.,-1.15470053837925));
#23936=CARTESIAN_POINT('',(2.07283766416844E-16,0.,-2.3094010767585));
#23937=CARTESIAN_POINT('',(2.,4.5,-1.15470053837925));
#23938=CARTESIAN_POINT('Origin',(2.,4.5,-1.15470053837925));
#23939=CARTESIAN_POINT('',(2.,0.,1.15470053837925));
#23940=CARTESIAN_POINT('',(2.,0.,-1.15470053837925));
#23941=CARTESIAN_POINT('',(2.,4.5,1.15470053837925));
#23942=CARTESIAN_POINT('Origin',(2.,4.5,1.15470053837925));
#23943=CARTESIAN_POINT('',(8.67361737988404E-16,0.,2.3094010767585));
#23944=CARTESIAN_POINT('',(2.,0.,1.15470053837925));
#23945=CARTESIAN_POINT('',(4.86323526963846E-16,4.5,2.3094010767585));
#23946=CARTESIAN_POINT('Origin',(4.86323526963846E-16,4.5,2.3094010767585));
#23947=CARTESIAN_POINT('',(4.86323526963846E-16,0.,2.3094010767585));
#23948=CARTESIAN_POINT('Origin',(-3.49999999999999,0.,0.));
#32967=UNCERTAINTY_MEASURE_WITH_UNIT(LENGTH_MEASURE(0.01),#33017,
'DISTANCE_ACCURACY_VALUE',
'Maximum model space distance between geometric entities at asserted c
onnectivities');
#32984=UNCERTAINTY_MEASURE_WITH_UNIT(LENGTH_MEASURE(0.01),#33017,
'DISTANCE_ACCURACY_VALUE',
'Maximum model space distance between geometric entities at asserted c
onnectivities');
#32999=(
GEOMETRIC_REPRESENTATION_CONTEXT(3)
GLOBAL_UNCERTAINTY_ASSIGNED_CONTEXT((#32967))
GLOBAL_UNIT_ASSIGNED_CONTEXT((#33017,#33019,#33020))
REPRESENTATION_CONTEXT('','3D')
);
#33016=(
GEOMETRIC_REPRESENTATION_CONTEXT(3)
GLOBAL_UNCERTAINTY_ASSIGNED_CONTEXT((#32984))
GLOBAL_UNIT_ASSIGNED_CONTEXT((#33017,#33019,#33020))
REPRESENTATION_CONTEXT('','3D')
);
#33017=(
LENGTH_UNIT()
NAMED_UNIT(*)
SI_UNIT(.MILLI.,.METRE.)
);
#33019=(
NAMED_UNIT(*)
PLANE_ANGLE_UNIT()
SI_UNIT($,.RADIAN.)
);
#33020=(
NAMED_UNIT(*)
SI_UNIT($,.STERADIAN.)
SOLID_ANGLE_UNIT()
);
#33035=SHAPE_DEFINITION_REPRESENTATION(#33074,#33138);
#33074=PRODUCT_DEFINITION_SHAPE('',$,#33170);
#33138=SHAPE_REPRESENTATION('',(#10782),#32999);
#33155=PRODUCT_DEFINITION_CONTEXT('part definition',#33250,'design');
#33170=PRODUCT_DEFINITION(
'P_Torque Wrench_Calibration Screw_PRT-TQ1012-10_M_Rev00',
'PRT-TQ1012-10',#33201,#33155);
#33201=PRODUCT_DEFINITION_FORMATION('',$,#33266);
#33250=APPLICATION_CONTEXT(
'Core Data for Automotive Mechanical Design Process');
#33251=PRODUCT_CONTEXT('part definition',#33250,'mechanical');
#33266=PRODUCT(
'P_Torque Wrench_Calibration Screw_PRT-TQ1012-10_M_Rev00',
'PRT-TQ1012-10',$,(#33251));
#33289=PRESENTATION_STYLE_ASSIGNMENT((#33296));
#33296=SURFACE_STYLE_USAGE(.BOTH.,#33303);
#33303=SURFACE_SIDE_STYLE('',(#33310));
#33310=SURFACE_STYLE_FILL_AREA(#33317);
#33317=FILL_AREA_STYLE('Opaque(255,255,255)',(#33324));
#33324=FILL_AREA_STYLE_COLOUR('Opaque(255,255,255)',#33331);
#33331=COLOUR_RGB('Opaque(255,255,255)', 0.08235294, 0.09019608, 0.10196078);
ENDSEC;
END-ISO-10303-21;
